ISO-10303-21;
HEADER;
/* Generated by software containing ST-Developer
 * from STEP Tools, Inc. (www.steptools.com) 
 */

FILE_DESCRIPTION(
/* description */ ('STEP AP214'),
/* implementation_level */ '2;1');

FILE_NAME(
/* name */ 'PRT-BL-RH-1004-05.step',
/* time_stamp */ '2026-10-07T12:49:37-07:00',
/* author */ (''),
/* organization */ (''),
/* preprocessor_version */ 'ST-DEVELOPER v20.2',
/* originating_system */ 'Autodesk Translation Framework v15.15.0.0',
/* authorisation */ '');

FILE_SCHEMA (('AUTOMOTIVE_DESIGN { 1 0 10303 214 3 1 1 }'));
ENDSEC;

DATA;
#10=MECHANICAL_DESIGN_GEOMETRIC_PRESENTATION_REPRESENTATION('',(#290),#33016);
#236=SHAPE_REPRESENTATION_RELATIONSHIP('SRR','None',#33129,#263);
#263=ADVANCED_BREP_SHAPE_REPRESENTATION('',(#321),#32990);
#290=STYLED_ITEM('',(#33284),#321);
#321=MANIFOLD_SOLID_BREP('Body1',#9945);
#351=CONICAL_SURFACE('',#10624,3.,0.785398163397447);
#352=CONICAL_SURFACE('',#10625,2.5,0.785398163397446);
#885=PLANE('',#10620);
#886=PLANE('',#10622);
#1233=FACE_OUTER_BOUND('',#1808,.T.);
#1234=FACE_OUTER_BOUND('',#1809,.T.);
#1235=FACE_OUTER_BOUND('',#1810,.T.);
#1236=FACE_OUTER_BOUND('',#1811,.T.);
#1237=FACE_OUTER_BOUND('',#1812,.T.);
#1808=EDGE_LOOP('',(#7570,#7571,#7572,#7573,#7574));
#1809=EDGE_LOOP('',(#7575));
#1810=EDGE_LOOP('',(#7576));
#1811=EDGE_LOOP('',(#7577,#7578,#7579,#7580,#7581));
#1812=EDGE_LOOP('',(#7582,#7583,#7584,#7585));
#2353=CIRCLE('',#10617,3.);
#2354=CIRCLE('',#10618,3.);
#2355=CIRCLE('',#10619,3.);
#2356=CIRCLE('',#10621,2.5);
#2357=CIRCLE('',#10623,2.5);
#2994=LINE('',#17980,#3744);
#2995=LINE('',#17989,#3745);
#2996=LINE('',#17991,#3746);
#3744=VECTOR('',#12331,3.);
#3745=VECTOR('',#12344,3.);
#3746=VECTOR('',#12347,2.5);
#4475=VERTEX_POINT('',#17975);
#4476=VERTEX_POINT('',#17976);
#4477=VERTEX_POINT('',#17979);
#4478=VERTEX_POINT('',#17983);
#4479=VERTEX_POINT('',#17986);
#5598=EDGE_CURVE('',#4475,#4476,#2353,.T.);
#5599=EDGE_CURVE('',#4476,#4475,#2354,.T.);
#5600=EDGE_CURVE('',#4475,#4477,#2994,.T.);
#5601=EDGE_CURVE('',#4477,#4477,#2355,.T.);
#5602=EDGE_CURVE('',#4478,#4478,#2356,.T.);
#5603=EDGE_CURVE('',#4479,#4479,#2357,.T.);
#5604=EDGE_CURVE('',#4476,#4479,#2995,.T.);
#5605=EDGE_CURVE('',#4477,#4478,#2996,.T.);
#7570=ORIENTED_EDGE('',*,*,#5598,.T.);
#7571=ORIENTED_EDGE('',*,*,#5599,.T.);
#7572=ORIENTED_EDGE('',*,*,#5600,.T.);
#7573=ORIENTED_EDGE('',*,*,#5601,.T.);
#7574=ORIENTED_EDGE('',*,*,#5600,.F.);
#7575=ORIENTED_EDGE('',*,*,#5602,.T.);
#7576=ORIENTED_EDGE('',*,*,#5603,.T.);
#7577=ORIENTED_EDGE('',*,*,#5598,.F.);
#7578=ORIENTED_EDGE('',*,*,#5599,.F.);
#7579=ORIENTED_EDGE('',*,*,#5604,.T.);
#7580=ORIENTED_EDGE('',*,*,#5603,.F.);
#7581=ORIENTED_EDGE('',*,*,#5604,.F.);
#7582=ORIENTED_EDGE('',*,*,#5601,.F.);
#7583=ORIENTED_EDGE('',*,*,#5605,.T.);
#7584=ORIENTED_EDGE('',*,*,#5602,.F.);
#7585=ORIENTED_EDGE('',*,*,#5605,.F.);
#9279=CYLINDRICAL_SURFACE('',#10616,3.);
#9599=ADVANCED_FACE('',(#1233),#9279,.T.);
#9600=ADVANCED_FACE('',(#1234),#885,.T.);
#9601=ADVANCED_FACE('',(#1235),#886,.F.);
#9602=ADVANCED_FACE('',(#1236),#351,.T.);
#9603=ADVANCED_FACE('',(#1237),#352,.T.);
#9945=CLOSED_SHELL('',(#9599,#9600,#9601,#9602,#9603));
#10615=AXIS2_PLACEMENT_3D('',#17973,#12323,#12324);
#10616=AXIS2_PLACEMENT_3D('',#17974,#12325,#12326);
#10617=AXIS2_PLACEMENT_3D('',#17977,#12327,#12328);
#10618=AXIS2_PLACEMENT_3D('',#17978,#12329,#12330);
#10619=AXIS2_PLACEMENT_3D('',#17981,#12332,#12333);
#10620=AXIS2_PLACEMENT_3D('',#17982,#12334,#12335);
#10621=AXIS2_PLACEMENT_3D('',#17984,#12336,#12337);
#10622=AXIS2_PLACEMENT_3D('',#17985,#12338,#12339);
#10623=AXIS2_PLACEMENT_3D('',#17987,#12340,#12341);
#10624=AXIS2_PLACEMENT_3D('',#17988,#12342,#12343);
#10625=AXIS2_PLACEMENT_3D('',#17990,#12345,#12346);
#12323=DIRECTION('axis',(0.,0.,1.));
#12324=DIRECTION('refdir',(1.,0.,0.));
#12325=DIRECTION('center_axis',(0.,-1.,0.));
#12326=DIRECTION('ref_axis',(0.,0.,-1.));
#12327=DIRECTION('center_axis',(0.,1.,0.));
#12328=DIRECTION('ref_axis',(0.,0.,1.));
#12329=DIRECTION('center_axis',(0.,1.,0.));
#12330=DIRECTION('ref_axis',(0.,0.,1.));
#12331=DIRECTION('',(0.,1.,0.));
#12332=DIRECTION('center_axis',(0.,-1.,0.));
#12333=DIRECTION('ref_axis',(0.,0.,1.));
#12334=DIRECTION('center_axis',(0.,1.,0.));
#12335=DIRECTION('ref_axis',(0.,0.,1.));
#12336=DIRECTION('center_axis',(0.,1.,0.));
#12337=DIRECTION('ref_axis',(0.,0.,1.));
#12338=DIRECTION('center_axis',(0.,1.,0.));
#12339=DIRECTION('ref_axis',(0.,0.,1.));
#12340=DIRECTION('center_axis',(0.,-1.,0.));
#12341=DIRECTION('ref_axis',(0.,0.,1.));
#12342=DIRECTION('center_axis',(0.,1.,0.));
#12343=DIRECTION('ref_axis',(0.,0.,1.));
#12344=DIRECTION('',(8.65956056235493E-17,-0.707106781186548,0.707106781186547));
#12345=DIRECTION('center_axis',(0.,-1.,0.));
#12346=DIRECTION('ref_axis',(0.,0.,-1.));
#12347=DIRECTION('',(8.65956056235491E-17,0.707106781186549,-0.707106781186546));
#17973=CARTESIAN_POINT('',(0.,0.,0.));
#17974=CARTESIAN_POINT('Origin',(0.,6.95,0.));
#17975=CARTESIAN_POINT('',(0.,-6.45,3.));
#17976=CARTESIAN_POINT('',(-3.67394039744206E-16,-6.45,-3.));
#17977=CARTESIAN_POINT('Origin',(0.,-6.45,0.));
#17978=CARTESIAN_POINT('Origin',(0.,-6.45,0.));
#17979=CARTESIAN_POINT('',(0.,6.45,3.));
#17980=CARTESIAN_POINT('',(-3.67394039744206E-16,6.95,3.));
#17981=CARTESIAN_POINT('Origin',(0.,6.45,0.));
#17982=CARTESIAN_POINT('Origin',(0.,6.95,0.));
#17983=CARTESIAN_POINT('',(0.,6.95,2.5));
#17984=CARTESIAN_POINT('Origin',(0.,6.95,0.));
#17985=CARTESIAN_POINT('Origin',(0.,-6.95,0.));
#17986=CARTESIAN_POINT('',(-3.06161699786838E-16,-6.95,-2.5));
#17987=CARTESIAN_POINT('Origin',(0.,-6.95,0.));
#17988=CARTESIAN_POINT('Origin',(0.,-6.45,0.));
#17989=CARTESIAN_POINT('',(-3.67394039744206E-16,-6.45,-3.));
#17990=CARTESIAN_POINT('Origin',(0.,6.95,0.));
#17991=CARTESIAN_POINT('',(-3.06161699786838E-16,6.95,2.5));
#32958=UNCERTAINTY_MEASURE_WITH_UNIT(LENGTH_MEASURE(0.01),#33017,
'DISTANCE_ACCURACY_VALUE',
'Maximum model space distance between geometric entities at asserted c
onnectivities');
#32984=UNCERTAINTY_MEASURE_WITH_UNIT(LENGTH_MEASURE(0.01),#33017,
'DISTANCE_ACCURACY_VALUE',
'Maximum model space distance between geometric entities at asserted c
onnectivities');
#32990=(
GEOMETRIC_REPRESENTATION_CONTEXT(3)
GLOBAL_UNCERTAINTY_ASSIGNED_CONTEXT((#32958))
GLOBAL_UNIT_ASSIGNED_CONTEXT((#33017,#33019,#33020))
REPRESENTATION_CONTEXT('','3D')
);
#33016=(
GEOMETRIC_REPRESENTATION_CONTEXT(3)
GLOBAL_UNCERTAINTY_ASSIGNED_CONTEXT((#32984))
GLOBAL_UNIT_ASSIGNED_CONTEXT((#33017,#33019,#33020))
REPRESENTATION_CONTEXT('','3D')
);
#33017=(
LENGTH_UNIT()
NAMED_UNIT(*)
SI_UNIT(.MILLI.,.METRE.)
);
#33019=(
NAMED_UNIT(*)
PLANE_ANGLE_UNIT()
SI_UNIT($,.RADIAN.)
);
#33020=(
NAMED_UNIT(*)
SI_UNIT($,.STERADIAN.)
SOLID_ANGLE_UNIT()
);
#33026=SHAPE_DEFINITION_REPRESENTATION(#33057,#33129);
#33057=PRODUCT_DEFINITION_SHAPE('',$,#33161);
#33129=SHAPE_REPRESENTATION('',(#10615),#32990);
#33155=PRODUCT_DEFINITION_CONTEXT('part definition',#33250,'design');
#33161=PRODUCT_DEFINITION(
'P_Torque Wrench_Pin_PRT-BL-RH-1004-05_M_Rev00','PRT-BL-RH-1004-05',#33192,
#33155);
#33192=PRODUCT_DEFINITION_FORMATION('',$,#33257);
#33250=APPLICATION_CONTEXT(
'Core Data for Automotive Mechanical Design Process');
#33251=PRODUCT_CONTEXT('part definition',#33250,'mechanical');
#33257=PRODUCT('P_Torque Wrench_Pin_PRT-BL-RH-1004-05_M_Rev00',
'PRT-BL-RH-1004-05',$,(#33251));
#33284=PRESENTATION_STYLE_ASSIGNMENT((#33291));
#33291=SURFACE_STYLE_USAGE(.BOTH.,#33298);
#33298=SURFACE_SIDE_STYLE('',(#33305));
#33305=SURFACE_STYLE_FILL_AREA(#33312);
#33312=FILL_AREA_STYLE('Opaque(186,91,6)',(#33319));
#33319=FILL_AREA_STYLE_COLOUR('Opaque(186,91,6)',#33326);
#33326=COLOUR_RGB('Opaque(186,91,6)', 0.09019608, 0.27058824, 0.51372549);
ENDSEC;
END-ISO-10303-21;
